ISO-10303-21;
HEADER;
/* Generated by software containing ST-Developer
 * from STEP Tools, Inc. (www.steptools.com) 
 */

FILE_DESCRIPTION(
/* description */ ('Independently dimensioned six-bar single-leg walking-linkage demonstr
ator. Whole-mm20 crank,60 upper rocker,80/120 ternary coupler,120 lowe
r rocker,140 knee pitch and260 toe reach; ground pivots0/0,60/0,40/60.
 Seven native revolutes close both loops. Four reused native library f
amilies, fully retained shared pins and layered real spacer stacks, bo
nded rubber toe. Benchtop reference mechanism; no complete vehicle, lo
ad, gait stability, adhesive, weld, fit or life rating.'),
/* implementation_level */ '2;1');

FILE_NAME(
/* name */ 'Back thrust washer.step',
/* time_stamp */ '2026-11-09T20:33:14-08:00',
/* author */ (''),
/* organization */ (''),
/* preprocessor_version */ 'ST-DEVELOPER v20.2',
/* originating_system */ 'Autodesk Translation Framework v15.17.0.0',
/* authorisation */ '');

FILE_SCHEMA (('AUTOMOTIVE_DESIGN { 1 0 10303 214 3 1 1 }'));
ENDSEC;

DATA;
#10=MECHANICAL_DESIGN_GEOMETRIC_PRESENTATION_REPRESENTATION('',(#271),#4048);
#235=SHAPE_REPRESENTATION_RELATIONSHIP('SRR','None',#4159,#253);
#253=ADVANCED_BREP_SHAPE_REPRESENTATION('',(#289),#4046);
#271=STYLED_ITEM('',(#4250),#289);
#289=MANIFOLD_SOLID_BREP('Body1',#2160);
#344=FACE_BOUND('',#715,.T.);
#345=FACE_BOUND('',#717,.T.);
#411=PLANE('',#2609);
#412=PLANE('',#2610);
#533=FACE_OUTER_BOUND('',#712,.T.);
#534=FACE_OUTER_BOUND('',#713,.T.);
#535=FACE_OUTER_BOUND('',#714,.T.);
#536=FACE_OUTER_BOUND('',#716,.T.);
#712=EDGE_LOOP('',(#1939,#1940,#1941,#1942));
#713=EDGE_LOOP('',(#1943,#1944,#1945,#1946));
#714=EDGE_LOOP('',(#1947));
#715=EDGE_LOOP('',(#1948));
#716=EDGE_LOOP('',(#1949));
#717=EDGE_LOOP('',(#1950));
#845=LINE('',#3933,#970);
#846=LINE('',#3939,#971);
#970=VECTOR('',#3280,5.);
#971=VECTOR('',#3287,10.);
#1080=CIRCLE('',#2604,5.);
#1081=CIRCLE('',#2605,5.);
#1082=CIRCLE('',#2607,10.);
#1083=CIRCLE('',#2608,10.);
#1238=VERTEX_POINT('',#3930);
#1239=VERTEX_POINT('',#3932);
#1240=VERTEX_POINT('',#3936);
#1241=VERTEX_POINT('',#3938);
#1473=EDGE_CURVE('',#1238,#1238,#1080,.T.);
#1474=EDGE_CURVE('',#1238,#1239,#845,.T.);
#1475=EDGE_CURVE('',#1239,#1239,#1081,.T.);
#1476=EDGE_CURVE('',#1240,#1240,#1082,.T.);
#1477=EDGE_CURVE('',#1240,#1241,#846,.T.);
#1478=EDGE_CURVE('',#1241,#1241,#1083,.T.);
#1939=ORIENTED_EDGE('',*,*,#1473,.F.);
#1940=ORIENTED_EDGE('',*,*,#1474,.T.);
#1941=ORIENTED_EDGE('',*,*,#1475,.T.);
#1942=ORIENTED_EDGE('',*,*,#1474,.F.);
#1943=ORIENTED_EDGE('',*,*,#1476,.F.);
#1944=ORIENTED_EDGE('',*,*,#1477,.T.);
#1945=ORIENTED_EDGE('',*,*,#1478,.T.);
#1946=ORIENTED_EDGE('',*,*,#1477,.F.);
#1947=ORIENTED_EDGE('',*,*,#1476,.T.);
#1948=ORIENTED_EDGE('',*,*,#1473,.T.);
#1949=ORIENTED_EDGE('',*,*,#1478,.F.);
#1950=ORIENTED_EDGE('',*,*,#1475,.F.);
#2014=CYLINDRICAL_SURFACE('',#2603,5.);
#2015=CYLINDRICAL_SURFACE('',#2606,10.);
#2136=ADVANCED_FACE('',(#533),#2014,.F.);
#2137=ADVANCED_FACE('',(#534),#2015,.T.);
#2138=ADVANCED_FACE('',(#535,#344),#411,.T.);
#2139=ADVANCED_FACE('',(#536,#345),#412,.F.);
#2160=CLOSED_SHELL('',(#2136,#2137,#2138,#2139));
#2602=AXIS2_PLACEMENT_3D('',#3928,#3274,#3275);
#2603=AXIS2_PLACEMENT_3D('',#3929,#3276,#3277);
#2604=AXIS2_PLACEMENT_3D('',#3931,#3278,#3279);
#2605=AXIS2_PLACEMENT_3D('',#3934,#3281,#3282);
#2606=AXIS2_PLACEMENT_3D('',#3935,#3283,#3284);
#2607=AXIS2_PLACEMENT_3D('',#3937,#3285,#3286);
#2608=AXIS2_PLACEMENT_3D('',#3940,#3288,#3289);
#2609=AXIS2_PLACEMENT_3D('',#3941,#3290,#3291);
#2610=AXIS2_PLACEMENT_3D('',#3942,#3292,#3293);
#3274=DIRECTION('axis',(0.,0.,1.));
#3275=DIRECTION('refdir',(1.,0.,0.));
#3276=DIRECTION('center_axis',(0.,0.,1.));
#3277=DIRECTION('ref_axis',(1.,0.,0.));
#3278=DIRECTION('center_axis',(0.,0.,-1.));
#3279=DIRECTION('ref_axis',(1.,0.,0.));
#3280=DIRECTION('',(0.,0.,-1.));
#3281=DIRECTION('center_axis',(0.,0.,-1.));
#3282=DIRECTION('ref_axis',(1.,0.,0.));
#3283=DIRECTION('center_axis',(0.,0.,1.));
#3284=DIRECTION('ref_axis',(1.,0.,0.));
#3285=DIRECTION('center_axis',(0.,0.,1.));
#3286=DIRECTION('ref_axis',(1.,0.,0.));
#3287=DIRECTION('',(0.,0.,-1.));
#3288=DIRECTION('center_axis',(0.,0.,1.));
#3289=DIRECTION('ref_axis',(1.,0.,0.));
#3290=DIRECTION('center_axis',(0.,0.,1.));
#3291=DIRECTION('ref_axis',(1.,0.,0.));
#3292=DIRECTION('center_axis',(0.,0.,1.));
#3293=DIRECTION('ref_axis',(1.,0.,0.));
#3928=CARTESIAN_POINT('',(0.,0.,0.));
#3929=CARTESIAN_POINT('Origin',(0.,0.,0.));
#3930=CARTESIAN_POINT('',(-5.,-6.12323399573677E-16,1.));
#3931=CARTESIAN_POINT('Origin',(0.,0.,1.));
#3932=CARTESIAN_POINT('',(-5.,-6.12323399573677E-16,0.));
#3933=CARTESIAN_POINT('',(-5.,-6.12323399573677E-16,0.));
#3934=CARTESIAN_POINT('Origin',(0.,0.,0.));
#3935=CARTESIAN_POINT('Origin',(0.,0.,0.));
#3936=CARTESIAN_POINT('',(-10.,-1.22464679914735E-15,1.));
#3937=CARTESIAN_POINT('Origin',(0.,0.,1.));
#3938=CARTESIAN_POINT('',(-10.,-1.22464679914735E-15,0.));
#3939=CARTESIAN_POINT('',(-10.,-1.22464679914735E-15,0.));
#3940=CARTESIAN_POINT('Origin',(0.,0.,0.));
#3941=CARTESIAN_POINT('Origin',(0.,0.,1.));
#3942=CARTESIAN_POINT('Origin',(0.,0.,0.));
#4026=UNCERTAINTY_MEASURE_WITH_UNIT(LENGTH_MEASURE(0.01),#4049,
'DISTANCE_ACCURACY_VALUE',
'Maximum model space distance between geometric entities at asserted c
onnectivities');
#4028=UNCERTAINTY_MEASURE_WITH_UNIT(LENGTH_MEASURE(0.01),#4049,
'DISTANCE_ACCURACY_VALUE',
'Maximum model space distance between geometric entities at asserted c
onnectivities');
#4046=(
GEOMETRIC_REPRESENTATION_CONTEXT(3)
GLOBAL_UNCERTAINTY_ASSIGNED_CONTEXT((#4026))
GLOBAL_UNIT_ASSIGNED_CONTEXT((#4049,#4051,#4052))
REPRESENTATION_CONTEXT('','3D')
);
#4048=(
GEOMETRIC_REPRESENTATION_CONTEXT(3)
GLOBAL_UNCERTAINTY_ASSIGNED_CONTEXT((#4028))
GLOBAL_UNIT_ASSIGNED_CONTEXT((#4049,#4051,#4052))
REPRESENTATION_CONTEXT('','3D')
);
#4049=(
LENGTH_UNIT()
NAMED_UNIT(*)
SI_UNIT(.MILLI.,.METRE.)
);
#4051=(
NAMED_UNIT(*)
PLANE_ANGLE_UNIT()
SI_UNIT($,.RADIAN.)
);
#4052=(
NAMED_UNIT(*)
SI_UNIT($,.STERADIAN.)
SOLID_ANGLE_UNIT()
);
#4070=SHAPE_DEFINITION_REPRESENTATION(#4089,#4159);
#4089=PRODUCT_DEFINITION_SHAPE('',$,#4179);
#4159=SHAPE_REPRESENTATION('',(#2602),#4046);
#4161=PRODUCT_DEFINITION_CONTEXT('part definition',#4220,'design');
#4179=PRODUCT_DEFINITION('Back thrust washer','Back thrust washer',#4198,
#4161);
#4198=PRODUCT_DEFINITION_FORMATION('',$,#4239);
#4220=APPLICATION_CONTEXT(
'Core Data for Automotive Mechanical Design Process');
#4221=PRODUCT_CONTEXT('part definition',#4220,'mechanical');
#4239=PRODUCT('Back thrust washer','Back thrust washer',$,(#4221));
#4250=PRESENTATION_STYLE_ASSIGNMENT((#4264));
#4264=SURFACE_STYLE_USAGE(.BOTH.,#4278);
#4278=SURFACE_SIDE_STYLE('',(#4292));
#4292=SURFACE_STYLE_FILL_AREA(#4306);
#4306=FILL_AREA_STYLE('Bearing light gray',(#4320));
#4320=FILL_AREA_STYLE_COLOUR('Bearing light gray',#4334);
#4334=COLOUR_RGB('Bearing light gray',0.725490196078431,0.752941176470588,
0.792156862745098);
ENDSEC;
END-ISO-10303-21;
